ISO-10303-21;
HEADER;
/* Generated by software containing ST-Developer
 * from STEP Tools, Inc. (www.steptools.com) 
 */

FILE_DESCRIPTION(
/* description */ ('Turntable on roller ring'),
/* implementation_level */ '2;1');

FILE_NAME(
/* name */ 'Outer race retainer (7).step',
/* time_stamp */ '2026-10-28T03:23:59-07:00',
/* author */ (''),
/* organization */ (''),
/* preprocessor_version */ 'ST-DEVELOPER v20.2',
/* originating_system */ 'Autodesk Translation Framework v15.17.0.0',
/* authorisation */ '');

FILE_SCHEMA (('AUTOMOTIVE_DESIGN { 1 0 10303 214 3 1 1 }'));
ENDSEC;

DATA;
#10=MECHANICAL_DESIGN_GEOMETRIC_PRESENTATION_REPRESENTATION('',(#675),#16281);
#556=SHAPE_REPRESENTATION_RELATIONSHIP('SRR','None',#16580,#611);
#611=ADVANCED_BREP_SHAPE_REPRESENTATION('',(#743),#16274);
#675=STYLED_ITEM('',(#16932),#743);
#743=MANIFOLD_SOLID_BREP('Body1',#8420);
#979=FACE_BOUND('',#2430,.T.);
#980=FACE_BOUND('',#2432,.T.);
#1231=PLANE('',#10038);
#1232=PLANE('',#10039);
#1700=FACE_OUTER_BOUND('',#2427,.T.);
#1701=FACE_OUTER_BOUND('',#2428,.T.);
#1702=FACE_OUTER_BOUND('',#2429,.T.);
#1703=FACE_OUTER_BOUND('',#2431,.T.);
#2427=EDGE_LOOP('',(#7445,#7446,#7447,#7448));
#2428=EDGE_LOOP('',(#7449,#7450,#7451,#7452));
#2429=EDGE_LOOP('',(#7453));
#2430=EDGE_LOOP('',(#7454));
#2431=EDGE_LOOP('',(#7455));
#2432=EDGE_LOOP('',(#7456));
#2958=LINE('',#15522,#3441);
#2959=LINE('',#15528,#3442);
#3441=VECTOR('',#12653,1.1);
#3442=VECTOR('',#12660,1.5);
#3873=CIRCLE('',#10033,1.1);
#3874=CIRCLE('',#10034,1.1);
#3875=CIRCLE('',#10036,1.5);
#3876=CIRCLE('',#10037,1.5);
#4549=VERTEX_POINT('',#15519);
#4550=VERTEX_POINT('',#15521);
#4551=VERTEX_POINT('',#15525);
#4552=VERTEX_POINT('',#15527);
#5533=EDGE_CURVE('',#4549,#4549,#3873,.T.);
#5534=EDGE_CURVE('',#4549,#4550,#2958,.T.);
#5535=EDGE_CURVE('',#4550,#4550,#3874,.T.);
#5536=EDGE_CURVE('',#4551,#4551,#3875,.T.);
#5537=EDGE_CURVE('',#4551,#4552,#2959,.T.);
#5538=EDGE_CURVE('',#4552,#4552,#3876,.T.);
#7445=ORIENTED_EDGE('',*,*,#5533,.F.);
#7446=ORIENTED_EDGE('',*,*,#5534,.T.);
#7447=ORIENTED_EDGE('',*,*,#5535,.T.);
#7448=ORIENTED_EDGE('',*,*,#5534,.F.);
#7449=ORIENTED_EDGE('',*,*,#5536,.F.);
#7450=ORIENTED_EDGE('',*,*,#5537,.T.);
#7451=ORIENTED_EDGE('',*,*,#5538,.T.);
#7452=ORIENTED_EDGE('',*,*,#5537,.F.);
#7453=ORIENTED_EDGE('',*,*,#5536,.T.);
#7454=ORIENTED_EDGE('',*,*,#5533,.T.);
#7455=ORIENTED_EDGE('',*,*,#5538,.F.);
#7456=ORIENTED_EDGE('',*,*,#5535,.F.);
#7839=CYLINDRICAL_SURFACE('',#10032,1.1);
#7840=CYLINDRICAL_SURFACE('',#10035,1.5);
#8303=ADVANCED_FACE('',(#1700),#7839,.F.);
#8304=ADVANCED_FACE('',(#1701),#7840,.T.);
#8305=ADVANCED_FACE('',(#1702,#979),#1231,.T.);
#8306=ADVANCED_FACE('',(#1703,#980),#1232,.F.);
#8420=CLOSED_SHELL('',(#8303,#8304,#8305,#8306));
#10031=AXIS2_PLACEMENT_3D('',#15517,#12647,#12648);
#10032=AXIS2_PLACEMENT_3D('',#15518,#12649,#12650);
#10033=AXIS2_PLACEMENT_3D('',#15520,#12651,#12652);
#10034=AXIS2_PLACEMENT_3D('',#15523,#12654,#12655);
#10035=AXIS2_PLACEMENT_3D('',#15524,#12656,#12657);
#10036=AXIS2_PLACEMENT_3D('',#15526,#12658,#12659);
#10037=AXIS2_PLACEMENT_3D('',#15529,#12661,#12662);
#10038=AXIS2_PLACEMENT_3D('',#15530,#12663,#12664);
#10039=AXIS2_PLACEMENT_3D('',#15531,#12665,#12666);
#12647=DIRECTION('axis',(0.,0.,1.));
#12648=DIRECTION('refdir',(1.,0.,0.));
#12649=DIRECTION('center_axis',(0.,1.,0.));
#12650=DIRECTION('ref_axis',(1.,0.,0.));
#12651=DIRECTION('center_axis',(0.,-1.,0.));
#12652=DIRECTION('ref_axis',(1.,0.,0.));
#12653=DIRECTION('',(0.,-1.,0.));
#12654=DIRECTION('center_axis',(0.,-1.,0.));
#12655=DIRECTION('ref_axis',(1.,0.,0.));
#12656=DIRECTION('center_axis',(0.,1.,0.));
#12657=DIRECTION('ref_axis',(1.,0.,0.));
#12658=DIRECTION('center_axis',(0.,1.,0.));
#12659=DIRECTION('ref_axis',(1.,0.,0.));
#12660=DIRECTION('',(0.,-1.,0.));
#12661=DIRECTION('center_axis',(0.,1.,0.));
#12662=DIRECTION('ref_axis',(1.,0.,0.));
#12663=DIRECTION('center_axis',(0.,1.,0.));
#12664=DIRECTION('ref_axis',(1.,0.,0.));
#12665=DIRECTION('center_axis',(0.,1.,0.));
#12666=DIRECTION('ref_axis',(1.,0.,0.));
#15517=CARTESIAN_POINT('',(0.,0.,0.));
#15518=CARTESIAN_POINT('Origin',(0.,15.45,3.5));
#15519=CARTESIAN_POINT('',(-1.1,15.65,3.5));
#15520=CARTESIAN_POINT('Origin',(0.,15.65,3.5));
#15521=CARTESIAN_POINT('',(-1.1,15.45,3.5));
#15522=CARTESIAN_POINT('',(-1.1,15.45,3.5));
#15523=CARTESIAN_POINT('Origin',(0.,15.45,3.5));
#15524=CARTESIAN_POINT('Origin',(0.,15.45,3.5));
#15525=CARTESIAN_POINT('',(-1.5,15.65,3.5));
#15526=CARTESIAN_POINT('Origin',(0.,15.65,3.5));
#15527=CARTESIAN_POINT('',(-1.5,15.45,3.5));
#15528=CARTESIAN_POINT('',(-1.5,15.45,3.5));
#15529=CARTESIAN_POINT('Origin',(0.,15.45,3.5));
#15530=CARTESIAN_POINT('Origin',(0.,15.65,3.5));
#15531=CARTESIAN_POINT('Origin',(0.,15.45,3.5));
#16205=UNCERTAINTY_MEASURE_WITH_UNIT(LENGTH_MEASURE(0.001),#16282,
'DISTANCE_ACCURACY_VALUE',
'Maximum model space distance between geometric entities at asserted c
onnectivities');
#16212=UNCERTAINTY_MEASURE_WITH_UNIT(LENGTH_MEASURE(0.001),#16282,
'DISTANCE_ACCURACY_VALUE',
'Maximum model space distance between geometric entities at asserted c
onnectivities');
#16274=(
GEOMETRIC_REPRESENTATION_CONTEXT(3)
GLOBAL_UNCERTAINTY_ASSIGNED_CONTEXT((#16205))
GLOBAL_UNIT_ASSIGNED_CONTEXT((#16282,#16284,#16285))
REPRESENTATION_CONTEXT('','3D')
);
#16281=(
GEOMETRIC_REPRESENTATION_CONTEXT(3)
GLOBAL_UNCERTAINTY_ASSIGNED_CONTEXT((#16212))
GLOBAL_UNIT_ASSIGNED_CONTEXT((#16282,#16284,#16285))
REPRESENTATION_CONTEXT('','3D')
);
#16282=(
LENGTH_UNIT()
NAMED_UNIT(*)
SI_UNIT(.CENTI.,.METRE.)
);
#16284=(
NAMED_UNIT(*)
PLANE_ANGLE_UNIT()
SI_UNIT($,.RADIAN.)
);
#16285=(
NAMED_UNIT(*)
SI_UNIT($,.STERADIAN.)
SOLID_ANGLE_UNIT()
);
#16347=SHAPE_DEFINITION_REPRESENTATION(#16481,#16580);
#16481=PRODUCT_DEFINITION_SHAPE('',$,#16649);
#16580=SHAPE_REPRESENTATION('',(#10031),#16274);
#16587=PRODUCT_DEFINITION_CONTEXT('part definition',#16793,'design');
#16649=PRODUCT_DEFINITION('Outer race retainer (7)',
'Outer race retainer (7)',#16717,#16587);
#16717=PRODUCT_DEFINITION_FORMATION('',$,#16856);
#16793=APPLICATION_CONTEXT(
'Core Data for Automotive Mechanical Design Process');
#16794=PRODUCT_CONTEXT('part definition',#16793,'mechanical');
#16856=PRODUCT('Outer race retainer (7)','Outer race retainer (7)',
'Outer race retainer (7)',(#16794));
#16926=COLOUR_RGB('Grey',0.48,0.52,0.57);
#16927=FILL_AREA_STYLE_COLOUR('',#16926);
#16928=FILL_AREA_STYLE('',(#16927));
#16929=SURFACE_STYLE_FILL_AREA(#16928);
#16930=SURFACE_SIDE_STYLE('',(#16929));
#16931=SURFACE_STYLE_USAGE(.BOTH.,#16930);
#16932=PRESENTATION_STYLE_ASSIGNMENT((#16931));
ENDSEC;
END-ISO-10303-21;
